ISO-10303-21;
HEADER;
/* Generated by software containing ST-Developer
 * from STEP Tools, Inc. (www.steptools.com) 
 */

FILE_DESCRIPTION(
/* description */ ('PAT-065'),
/* implementation_level */ '2;1');

FILE_NAME(
/* name */ 'Hex Nut - M8.step',
/* time_stamp */ '2026-10-28T22:09:22-07:00',
/* author */ (''),
/* organization */ (''),
/* preprocessor_version */ 'ST-DEVELOPER v20.2',
/* originating_system */ 'Autodesk Translation Framework v15.17.0.0',
/* authorisation */ '');

FILE_SCHEMA (('AUTOMOTIVE_DESIGN { 1 0 10303 214 3 1 1 }'));
ENDSEC;

DATA;
#10=MECHANICAL_DESIGN_GEOMETRIC_PRESENTATION_REPRESENTATION('',(#165),#5502);
#11=(
BOUNDED_CURVE()
B_SPLINE_CURVE(2,(#5238,#5239,#5240),.UNSPECIFIED.,.F.,.F.)
B_SPLINE_CURVE_WITH_KNOTS((3,3),(0.14973948338295,0.97160236658079),
 .UNSPECIFIED.)
CURVE()
GEOMETRIC_REPRESENTATION_ITEM()
RATIONAL_B_SPLINE_CURVE((1.07140024848292,1.23714644374248,1.07140024848292))
REPRESENTATION_ITEM('')
);
#12=(
BOUNDED_CURVE()
B_SPLINE_CURVE(2,(#5242,#5243,#5244),.UNSPECIFIED.,.F.,.F.)
B_SPLINE_CURVE_WITH_KNOTS((3,3),(0.14973948338295,0.971602366580789),
 .UNSPECIFIED.)
CURVE()
GEOMETRIC_REPRESENTATION_ITEM()
RATIONAL_B_SPLINE_CURVE((1.07140024848292,1.23714644374248,1.07140024848292))
REPRESENTATION_ITEM('')
);
#13=(
BOUNDED_CURVE()
B_SPLINE_CURVE(2,(#5249,#5250,#5251),.UNSPECIFIED.,.F.,.F.)
B_SPLINE_CURVE_WITH_KNOTS((3,3),(0.14973948338295,0.97160236658079),
 .UNSPECIFIED.)
CURVE()
GEOMETRIC_REPRESENTATION_ITEM()
RATIONAL_B_SPLINE_CURVE((1.07140024848292,1.23714644374248,1.07140024848292))
REPRESENTATION_ITEM('')
);
#14=(
BOUNDED_CURVE()
B_SPLINE_CURVE(2,(#5253,#5254,#5255),.UNSPECIFIED.,.F.,.F.)
B_SPLINE_CURVE_WITH_KNOTS((3,3),(0.14973948338295,0.97160236658079),
 .UNSPECIFIED.)
CURVE()
GEOMETRIC_REPRESENTATION_ITEM()
RATIONAL_B_SPLINE_CURVE((1.07140024848292,1.23714644374248,1.07140024848292))
REPRESENTATION_ITEM('')
);
#15=(
BOUNDED_CURVE()
B_SPLINE_CURVE(2,(#5257,#5258,#5259),.UNSPECIFIED.,.F.,.F.)
B_SPLINE_CURVE_WITH_KNOTS((3,3),(0.14973948338295,0.971602366580789),
 .UNSPECIFIED.)
CURVE()
GEOMETRIC_REPRESENTATION_ITEM()
RATIONAL_B_SPLINE_CURVE((1.07140024848292,1.23714644374248,1.07140024848292))
REPRESENTATION_ITEM('')
);
#16=(
BOUNDED_CURVE()
B_SPLINE_CURVE(2,(#5260,#5261,#5262),.UNSPECIFIED.,.F.,.F.)
B_SPLINE_CURVE_WITH_KNOTS((3,3),(0.14973948338295,0.97160236658079),
 .UNSPECIFIED.)
CURVE()
GEOMETRIC_REPRESENTATION_ITEM()
RATIONAL_B_SPLINE_CURVE((1.07140024848292,1.23714644374248,1.07140024848292))
REPRESENTATION_ITEM('')
);
#17=(
BOUNDED_CURVE()
B_SPLINE_CURVE(2,(#5269,#5270,#5271),.UNSPECIFIED.,.F.,.F.)
B_SPLINE_CURVE_WITH_KNOTS((3,3),(0.14973948338295,0.97160236658079),
 .UNSPECIFIED.)
CURVE()
GEOMETRIC_REPRESENTATION_ITEM()
RATIONAL_B_SPLINE_CURVE((1.07140024848292,1.23714644374248,1.07140024848292))
REPRESENTATION_ITEM('')
);
#18=(
BOUNDED_CURVE()
B_SPLINE_CURVE(2,(#5273,#5274,#5275),.UNSPECIFIED.,.F.,.F.)
B_SPLINE_CURVE_WITH_KNOTS((3,3),(0.14973948338295,0.97160236658079),
 .UNSPECIFIED.)
CURVE()
GEOMETRIC_REPRESENTATION_ITEM()
RATIONAL_B_SPLINE_CURVE((1.07140024848292,1.23714644374248,1.07140024848292))
REPRESENTATION_ITEM('')
);
#19=(
BOUNDED_CURVE()
B_SPLINE_CURVE(2,(#5277,#5278,#5279),.UNSPECIFIED.,.F.,.F.)
B_SPLINE_CURVE_WITH_KNOTS((3,3),(0.14973948338295,0.971602366580789),
 .UNSPECIFIED.)
CURVE()
GEOMETRIC_REPRESENTATION_ITEM()
RATIONAL_B_SPLINE_CURVE((1.07140024848292,1.23714644374248,1.07140024848292))
REPRESENTATION_ITEM('')
);
#20=(
BOUNDED_CURVE()
B_SPLINE_CURVE(2,(#5281,#5282,#5283),.UNSPECIFIED.,.F.,.F.)
B_SPLINE_CURVE_WITH_KNOTS((3,3),(0.14973948338295,0.97160236658079),
 .UNSPECIFIED.)
CURVE()
GEOMETRIC_REPRESENTATION_ITEM()
RATIONAL_B_SPLINE_CURVE((1.07140024848292,1.23714644374248,1.07140024848292))
REPRESENTATION_ITEM('')
);
#21=(
BOUNDED_CURVE()
B_SPLINE_CURVE(2,(#5285,#5286,#5287),.UNSPECIFIED.,.F.,.F.)
B_SPLINE_CURVE_WITH_KNOTS((3,3),(0.14973948338295,0.97160236658079),
 .UNSPECIFIED.)
CURVE()
GEOMETRIC_REPRESENTATION_ITEM()
RATIONAL_B_SPLINE_CURVE((1.07140024848292,1.23714644374248,1.07140024848292))
REPRESENTATION_ITEM('')
);
#22=(
BOUNDED_CURVE()
B_SPLINE_CURVE(2,(#5288,#5289,#5290),.UNSPECIFIED.,.F.,.F.)
B_SPLINE_CURVE_WITH_KNOTS((3,3),(0.14973948338295,0.971602366580789),
 .UNSPECIFIED.)
CURVE()
GEOMETRIC_REPRESENTATION_ITEM()
RATIONAL_B_SPLINE_CURVE((1.07140024848292,1.23714644374248,1.07140024848292))
REPRESENTATION_ITEM('')
);
#124=CONICAL_SURFACE('',#3534,0.734027674973257,1.0471975511966);
#125=CONICAL_SURFACE('',#3536,0.734027674973257,1.0471975511966);
#145=SHAPE_REPRESENTATION_RELATIONSHIP('SRR','None',#5563,#155);
#155=ADVANCED_BREP_SHAPE_REPRESENTATION('',(#174),#5499);
#165=STYLED_ITEM('',(#5701),#174);
#174=MANIFOLD_SOLID_BREP('Body1',#3213);
#195=FACE_BOUND('',#660,.T.);
#196=FACE_BOUND('',#662,.T.);
#197=FACE_BOUND('',#674,.T.);
#198=FACE_BOUND('',#676,.T.);
#304=PLANE('',#3528);
#305=PLANE('',#3530);
#306=PLANE('',#3538);
#307=PLANE('',#3539);
#308=PLANE('',#3540);
#309=PLANE('',#3543);
#310=PLANE('',#3544);
#311=PLANE('',#3545);
#312=PLANE('',#3546);
#313=PLANE('',#3547);
#466=FACE_OUTER_BOUND('',#658,.T.);
#467=FACE_OUTER_BOUND('',#659,.T.);
#468=FACE_OUTER_BOUND('',#661,.T.);
#469=FACE_OUTER_BOUND('',#663,.T.);
#470=FACE_OUTER_BOUND('',#664,.T.);
#471=FACE_OUTER_BOUND('',#665,.T.);
#472=FACE_OUTER_BOUND('',#666,.T.);
#473=FACE_OUTER_BOUND('',#667,.T.);
#474=FACE_OUTER_BOUND('',#668,.T.);
#475=FACE_OUTER_BOUND('',#669,.T.);
#476=FACE_OUTER_BOUND('',#670,.T.);
#477=FACE_OUTER_BOUND('',#671,.T.);
#478=FACE_OUTER_BOUND('',#672,.T.);
#479=FACE_OUTER_BOUND('',#673,.T.);
#480=FACE_OUTER_BOUND('',#675,.T.);
#658=EDGE_LOOP('',(#2802,#2803,#2804,#2805));
#659=EDGE_LOOP('',(#2806));
#660=EDGE_LOOP('',(#2807));
#661=EDGE_LOOP('',(#2808));
#662=EDGE_LOOP('',(#2809));
#663=EDGE_LOOP('',(#2810,#2811,#2812,#2813));
#664=EDGE_LOOP('',(#2814,#2815,#2816,#2817,#2818,#2819,#2820,#2821,#2822));
#665=EDGE_LOOP('',(#2823,#2824,#2825,#2826,#2827,#2828,#2829,#2830,#2831));
#666=EDGE_LOOP('',(#2832,#2833,#2834,#2835));
#667=EDGE_LOOP('',(#2836,#2837,#2838,#2839));
#668=EDGE_LOOP('',(#2840,#2841,#2842,#2843));
#669=EDGE_LOOP('',(#2844,#2845,#2846,#2847));
#670=EDGE_LOOP('',(#2848,#2849,#2850,#2851));
#671=EDGE_LOOP('',(#2852,#2853,#2854,#2855));
#672=EDGE_LOOP('',(#2856,#2857,#2858,#2859));
#673=EDGE_LOOP('',(#2860));
#674=EDGE_LOOP('',(#2861));
#675=EDGE_LOOP('',(#2862));
#676=EDGE_LOOP('',(#2863));
#977=LINE('',#5223,#1308);
#978=LINE('',#5233,#1309);
#979=LINE('',#5246,#1310);
#980=LINE('',#5267,#1311);
#981=LINE('',#5292,#1312);
#982=LINE('',#5293,#1313);
#983=LINE('',#5295,#1314);
#984=LINE('',#5297,#1315);
#985=LINE('',#5301,#1316);
#986=LINE('',#5303,#1317);
#987=LINE('',#5305,#1318);
#1308=VECTOR('',#4286,0.5);
#1309=VECTOR('',#4299,0.4);
#1310=VECTOR('',#4304,0.734027674973257);
#1311=VECTOR('',#4311,0.734027674973257);
#1312=VECTOR('',#4314,1.);
#1313=VECTOR('',#4315,1.);
#1314=VECTOR('',#4318,1.);
#1315=VECTOR('',#4321,1.);
#1316=VECTOR('',#4326,0.4);
#1317=VECTOR('',#4329,1.);
#1318=VECTOR('',#4332,1.);
#1423=CIRCLE('',#3526,0.5);
#1424=CIRCLE('',#3527,0.5);
#1425=CIRCLE('',#3529,0.338975);
#1426=CIRCLE('',#3531,0.338975);
#1427=CIRCLE('',#3533,0.338975);
#1428=CIRCLE('',#3535,0.6175);
#1429=CIRCLE('',#3537,0.6175);
#1430=CIRCLE('',#3542,0.338975);
#1660=VERTEX_POINT('',#5220);
#1661=VERTEX_POINT('',#5222);
#1662=VERTEX_POINT('',#5226);
#1663=VERTEX_POINT('',#5229);
#1664=VERTEX_POINT('',#5232);
#1665=VERTEX_POINT('',#5236);
#1666=VERTEX_POINT('',#5237);
#1667=VERTEX_POINT('',#5241);
#1668=VERTEX_POINT('',#5245);
#1669=VERTEX_POINT('',#5248);
#1670=VERTEX_POINT('',#5252);
#1671=VERTEX_POINT('',#5256);
#1672=VERTEX_POINT('',#5264);
#1673=VERTEX_POINT('',#5266);
#1674=VERTEX_POINT('',#5268);
#1675=VERTEX_POINT('',#5272);
#1676=VERTEX_POINT('',#5276);
#1677=VERTEX_POINT('',#5280);
#1678=VERTEX_POINT('',#5284);
#1679=VERTEX_POINT('',#5299);
#2051=EDGE_CURVE('',#1660,#1660,#1423,.T.);
#2052=EDGE_CURVE('',#1660,#1661,#977,.T.);
#2053=EDGE_CURVE('',#1661,#1661,#1424,.T.);
#2054=EDGE_CURVE('',#1662,#1662,#1425,.T.);
#2055=EDGE_CURVE('',#1663,#1663,#1426,.T.);
#2056=EDGE_CURVE('',#1663,#1664,#978,.T.);
#2057=EDGE_CURVE('',#1664,#1664,#1427,.F.);
#2058=EDGE_CURVE('',#1665,#1666,#11,.T.);
#2059=EDGE_CURVE('',#1667,#1665,#12,.T.);
#2060=EDGE_CURVE('',#1667,#1668,#979,.T.);
#2061=EDGE_CURVE('',#1668,#1668,#1428,.T.);
#2062=EDGE_CURVE('',#1669,#1667,#13,.T.);
#2063=EDGE_CURVE('',#1670,#1669,#14,.T.);
#2064=EDGE_CURVE('',#1671,#1670,#15,.T.);
#2065=EDGE_CURVE('',#1666,#1671,#16,.T.);
#2066=EDGE_CURVE('',#1672,#1672,#1429,.T.);
#2067=EDGE_CURVE('',#1672,#1673,#980,.T.);
#2068=EDGE_CURVE('',#1674,#1673,#17,.T.);
#2069=EDGE_CURVE('',#1675,#1674,#18,.T.);
#2070=EDGE_CURVE('',#1676,#1675,#19,.T.);
#2071=EDGE_CURVE('',#1677,#1676,#20,.T.);
#2072=EDGE_CURVE('',#1678,#1677,#21,.T.);
#2073=EDGE_CURVE('',#1673,#1678,#22,.T.);
#2074=EDGE_CURVE('',#1669,#1678,#981,.T.);
#2075=EDGE_CURVE('',#1670,#1677,#982,.T.);
#2076=EDGE_CURVE('',#1667,#1673,#983,.T.);
#2077=EDGE_CURVE('',#1665,#1674,#984,.T.);
#2078=EDGE_CURVE('',#1679,#1679,#1430,.F.);
#2079=EDGE_CURVE('',#1679,#1662,#985,.T.);
#2080=EDGE_CURVE('',#1666,#1675,#986,.T.);
#2081=EDGE_CURVE('',#1671,#1676,#987,.T.);
#2802=ORIENTED_EDGE('',*,*,#2051,.F.);
#2803=ORIENTED_EDGE('',*,*,#2052,.T.);
#2804=ORIENTED_EDGE('',*,*,#2053,.T.);
#2805=ORIENTED_EDGE('',*,*,#2052,.F.);
#2806=ORIENTED_EDGE('',*,*,#2053,.F.);
#2807=ORIENTED_EDGE('',*,*,#2054,.F.);
#2808=ORIENTED_EDGE('',*,*,#2051,.T.);
#2809=ORIENTED_EDGE('',*,*,#2055,.F.);
#2810=ORIENTED_EDGE('',*,*,#2055,.T.);
#2811=ORIENTED_EDGE('',*,*,#2056,.T.);
#2812=ORIENTED_EDGE('',*,*,#2057,.T.);
#2813=ORIENTED_EDGE('',*,*,#2056,.F.);
#2814=ORIENTED_EDGE('',*,*,#2058,.F.);
#2815=ORIENTED_EDGE('',*,*,#2059,.F.);
#2816=ORIENTED_EDGE('',*,*,#2060,.T.);
#2817=ORIENTED_EDGE('',*,*,#2061,.F.);
#2818=ORIENTED_EDGE('',*,*,#2060,.F.);
#2819=ORIENTED_EDGE('',*,*,#2062,.F.);
#2820=ORIENTED_EDGE('',*,*,#2063,.F.);
#2821=ORIENTED_EDGE('',*,*,#2064,.F.);
#2822=ORIENTED_EDGE('',*,*,#2065,.F.);
#2823=ORIENTED_EDGE('',*,*,#2066,.F.);
#2824=ORIENTED_EDGE('',*,*,#2067,.T.);
#2825=ORIENTED_EDGE('',*,*,#2068,.F.);
#2826=ORIENTED_EDGE('',*,*,#2069,.F.);
#2827=ORIENTED_EDGE('',*,*,#2070,.F.);
#2828=ORIENTED_EDGE('',*,*,#2071,.F.);
#2829=ORIENTED_EDGE('',*,*,#2072,.F.);
#2830=ORIENTED_EDGE('',*,*,#2073,.F.);
#2831=ORIENTED_EDGE('',*,*,#2067,.F.);
#2832=ORIENTED_EDGE('',*,*,#2063,.T.);
#2833=ORIENTED_EDGE('',*,*,#2074,.T.);
#2834=ORIENTED_EDGE('',*,*,#2072,.T.);
#2835=ORIENTED_EDGE('',*,*,#2075,.F.);
#2836=ORIENTED_EDGE('',*,*,#2062,.T.);
#2837=ORIENTED_EDGE('',*,*,#2076,.T.);
#2838=ORIENTED_EDGE('',*,*,#2073,.T.);
#2839=ORIENTED_EDGE('',*,*,#2074,.F.);
#2840=ORIENTED_EDGE('',*,*,#2059,.T.);
#2841=ORIENTED_EDGE('',*,*,#2077,.T.);
#2842=ORIENTED_EDGE('',*,*,#2068,.T.);
#2843=ORIENTED_EDGE('',*,*,#2076,.F.);
#2844=ORIENTED_EDGE('',*,*,#2078,.F.);
#2845=ORIENTED_EDGE('',*,*,#2079,.T.);
#2846=ORIENTED_EDGE('',*,*,#2054,.T.);
#2847=ORIENTED_EDGE('',*,*,#2079,.F.);
#2848=ORIENTED_EDGE('',*,*,#2058,.T.);
#2849=ORIENTED_EDGE('',*,*,#2080,.T.);
#2850=ORIENTED_EDGE('',*,*,#2069,.T.);
#2851=ORIENTED_EDGE('',*,*,#2077,.F.);
#2852=ORIENTED_EDGE('',*,*,#2064,.T.);
#2853=ORIENTED_EDGE('',*,*,#2075,.T.);
#2854=ORIENTED_EDGE('',*,*,#2071,.T.);
#2855=ORIENTED_EDGE('',*,*,#2081,.F.);
#2856=ORIENTED_EDGE('',*,*,#2065,.T.);
#2857=ORIENTED_EDGE('',*,*,#2081,.T.);
#2858=ORIENTED_EDGE('',*,*,#2070,.T.);
#2859=ORIENTED_EDGE('',*,*,#2080,.F.);
#2860=ORIENTED_EDGE('',*,*,#2066,.T.);
#2861=ORIENTED_EDGE('',*,*,#2078,.T.);
#2862=ORIENTED_EDGE('',*,*,#2061,.T.);
#2863=ORIENTED_EDGE('',*,*,#2057,.F.);
#3023=CYLINDRICAL_SURFACE('',#3525,0.5);
#3024=CYLINDRICAL_SURFACE('',#3532,0.338975);
#3025=CYLINDRICAL_SURFACE('',#3541,0.338975);
#3160=ADVANCED_FACE('',(#466),#3023,.F.);
#3161=ADVANCED_FACE('',(#467,#195),#304,.F.);
#3162=ADVANCED_FACE('',(#468,#196),#305,.T.);
#3163=ADVANCED_FACE('',(#469),#3024,.F.);
#3164=ADVANCED_FACE('',(#470),#124,.T.);
#3165=ADVANCED_FACE('',(#471),#125,.T.);
#3166=ADVANCED_FACE('',(#472),#306,.T.);
#3167=ADVANCED_FACE('',(#473),#307,.T.);
#3168=ADVANCED_FACE('',(#474),#308,.T.);
#3169=ADVANCED_FACE('',(#475),#3025,.F.);
#3170=ADVANCED_FACE('',(#476),#309,.T.);
#3171=ADVANCED_FACE('',(#477),#310,.T.);
#3172=ADVANCED_FACE('',(#478),#311,.T.);
#3173=ADVANCED_FACE('',(#479,#197),#312,.T.);
#3174=ADVANCED_FACE('',(#480,#198),#313,.F.);
#3213=CLOSED_SHELL('',(#3160,#3161,#3162,#3163,#3164,#3165,#3166,#3167,
#3168,#3169,#3170,#3171,#3172,#3173,#3174));
#3524=AXIS2_PLACEMENT_3D('',#5218,#4280,#4281);
#3525=AXIS2_PLACEMENT_3D('',#5219,#4282,#4283);
#3526=AXIS2_PLACEMENT_3D('',#5221,#4284,#4285);
#3527=AXIS2_PLACEMENT_3D('',#5224,#4287,#4288);
#3528=AXIS2_PLACEMENT_3D('',#5225,#4289,#4290);
#3529=AXIS2_PLACEMENT_3D('',#5227,#4291,#4292);
#3530=AXIS2_PLACEMENT_3D('',#5228,#4293,#4294);
#3531=AXIS2_PLACEMENT_3D('',#5230,#4295,#4296);
#3532=AXIS2_PLACEMENT_3D('',#5231,#4297,#4298);
#3533=AXIS2_PLACEMENT_3D('',#5234,#4300,#4301);
#3534=AXIS2_PLACEMENT_3D('',#5235,#4302,#4303);
#3535=AXIS2_PLACEMENT_3D('',#5247,#4305,#4306);
#3536=AXIS2_PLACEMENT_3D('',#5263,#4307,#4308);
#3537=AXIS2_PLACEMENT_3D('',#5265,#4309,#4310);
#3538=AXIS2_PLACEMENT_3D('',#5291,#4312,#4313);
#3539=AXIS2_PLACEMENT_3D('',#5294,#4316,#4317);
#3540=AXIS2_PLACEMENT_3D('',#5296,#4319,#4320);
#3541=AXIS2_PLACEMENT_3D('',#5298,#4322,#4323);
#3542=AXIS2_PLACEMENT_3D('',#5300,#4324,#4325);
#3543=AXIS2_PLACEMENT_3D('',#5302,#4327,#4328);
#3544=AXIS2_PLACEMENT_3D('',#5304,#4330,#4331);
#3545=AXIS2_PLACEMENT_3D('',#5306,#4333,#4334);
#3546=AXIS2_PLACEMENT_3D('',#5307,#4335,#4336);
#3547=AXIS2_PLACEMENT_3D('',#5308,#4337,#4338);
#4280=DIRECTION('axis',(0.,0.,1.));
#4281=DIRECTION('refdir',(1.,0.,0.));
#4282=DIRECTION('center_axis',(0.,1.,0.));
#4283=DIRECTION('ref_axis',(1.,0.,0.));
#4284=DIRECTION('center_axis',(0.,1.,0.));
#4285=DIRECTION('ref_axis',(1.,0.,0.));
#4286=DIRECTION('',(0.,1.,0.));
#4287=DIRECTION('center_axis',(0.,1.,0.));
#4288=DIRECTION('ref_axis',(1.,0.,0.));
#4289=DIRECTION('center_axis',(0.,1.,0.));
#4290=DIRECTION('ref_axis',(1.,0.,0.));
#4291=DIRECTION('center_axis',(0.,-1.,0.));
#4292=DIRECTION('ref_axis',(1.,0.,0.));
#4293=DIRECTION('center_axis',(0.,1.,0.));
#4294=DIRECTION('ref_axis',(1.,0.,0.));
#4295=DIRECTION('center_axis',(0.,1.,0.));
#4296=DIRECTION('ref_axis',(1.,0.,0.));
#4297=DIRECTION('center_axis',(0.,1.,0.));
#4298=DIRECTION('ref_axis',(1.,0.,0.));
#4299=DIRECTION('',(0.,-1.,0.));
#4300=DIRECTION('center_axis',(0.,1.,0.));
#4301=DIRECTION('ref_axis',(1.,0.,0.));
#4302=DIRECTION('center_axis',(0.,1.,0.));
#4303=DIRECTION('ref_axis',(1.,0.,0.));
#4304=DIRECTION('',(0.866025403784439,-0.5,1.06057523872491E-16));
#4305=DIRECTION('center_axis',(0.,-1.,0.));
#4306=DIRECTION('ref_axis',(1.,0.,0.));
#4307=DIRECTION('center_axis',(0.,-1.,0.));
#4308=DIRECTION('ref_axis',(1.,0.,0.));
#4309=DIRECTION('center_axis',(0.,1.,0.));
#4310=DIRECTION('ref_axis',(1.,0.,0.));
#4311=DIRECTION('',(-0.866025403784439,-0.5,-1.06057523872491E-16));
#4312=DIRECTION('center_axis',(1.4792020664489E-16,0.,-1.));
#4313=DIRECTION('ref_axis',(-1.,0.,-1.4792020664489E-16));
#4314=DIRECTION('',(0.,1.,0.));
#4315=DIRECTION('',(0.,1.,0.));
#4316=DIRECTION('center_axis',(-0.866025403784439,0.,-0.5));
#4317=DIRECTION('ref_axis',(-0.5,0.,0.866025403784439));
#4318=DIRECTION('',(0.,1.,0.));
#4319=DIRECTION('center_axis',(-0.866025403784439,0.,0.5));
#4320=DIRECTION('ref_axis',(0.5,0.,0.866025403784439));
#4321=DIRECTION('',(0.,1.,0.));
#4322=DIRECTION('center_axis',(0.,1.,0.));
#4323=DIRECTION('ref_axis',(1.,0.,0.));
#4324=DIRECTION('center_axis',(0.,1.,0.));
#4325=DIRECTION('ref_axis',(1.,0.,0.));
#4326=DIRECTION('',(0.,-1.,0.));
#4327=DIRECTION('center_axis',(-2.95840413289779E-16,0.,1.));
#4328=DIRECTION('ref_axis',(1.,0.,2.95840413289779E-16));
#4329=DIRECTION('',(0.,1.,0.));
#4330=DIRECTION('center_axis',(0.866025403784439,0.,-0.5));
#4331=DIRECTION('ref_axis',(-0.5,0.,-0.866025403784439));
#4332=DIRECTION('',(0.,1.,0.));
#4333=DIRECTION('center_axis',(0.866025403784439,0.,0.5));
#4334=DIRECTION('ref_axis',(0.5,0.,-0.866025403784439));
#4335=DIRECTION('center_axis',(0.,1.,0.));
#4336=DIRECTION('ref_axis',(1.,0.,0.));
#4337=DIRECTION('center_axis',(0.,1.,0.));
#4338=DIRECTION('ref_axis',(1.,0.,0.));
#5218=CARTESIAN_POINT('',(0.,0.,0.));
#5219=CARTESIAN_POINT('Origin',(0.,0.2,0.));
#5220=CARTESIAN_POINT('',(-0.5,0.2,6.12323399573677E-17));
#5221=CARTESIAN_POINT('Origin',(0.,0.2,0.));
#5222=CARTESIAN_POINT('',(-0.5,0.6,6.12323399573677E-17));
#5223=CARTESIAN_POINT('',(-0.5,0.2,6.12323399573677E-17));
#5224=CARTESIAN_POINT('Origin',(0.,0.6,0.));
#5225=CARTESIAN_POINT('Origin',(0.,0.6,0.));
#5226=CARTESIAN_POINT('',(-0.338975,0.6,-4.15124648740974E-17));
#5227=CARTESIAN_POINT('Origin',(0.,0.6,0.));
#5228=CARTESIAN_POINT('Origin',(0.,0.2,0.));
#5229=CARTESIAN_POINT('',(-0.338975,0.2,4.15124648740974E-17));
#5230=CARTESIAN_POINT('Origin',(0.,0.2,0.));
#5231=CARTESIAN_POINT('Origin',(0.,0.,0.));
#5232=CARTESIAN_POINT('',(-0.338975,0.,4.15124648740974E-17));
#5233=CARTESIAN_POINT('',(-0.338975,0.,4.15124648740974E-17));
#5234=CARTESIAN_POINT('Origin',(0.,0.,0.));
#5235=CARTESIAN_POINT('Origin',(0.,0.067277284513851,0.));
#5236=CARTESIAN_POINT('',(-0.375277674973257,0.0768195421087395,0.65));
#5237=CARTESIAN_POINT('',(0.375277674973257,0.0768195421087395,0.65));
#5238=CARTESIAN_POINT('Ctrl Pts',(-0.375277674973257,0.0768195421087395,
0.65));
#5239=CARTESIAN_POINT('Ctrl Pts',(1.66533453693773E-13,-0.0315137912242439,
0.65));
#5240=CARTESIAN_POINT('Ctrl Pts',(0.375277674973257,0.0768195421087394,
0.65));
#5241=CARTESIAN_POINT('',(-0.750555349946514,0.0768195421087394,-9.19165206894919E-17));
#5242=CARTESIAN_POINT('Ctrl Pts',(-0.750555349946514,0.0768195421087394,
-9.19165206894919E-17));
#5243=CARTESIAN_POINT('Ctrl Pts',(-0.562916512459802,-0.0315137912242434,
0.325000000000144));
#5244=CARTESIAN_POINT('Ctrl Pts',(-0.375277674973257,0.0768195421087395,
0.65));
#5245=CARTESIAN_POINT('',(-0.6175,-2.77555756156289E-17,-7.5621939847349E-17));
#5246=CARTESIAN_POINT('',(-0.734027674973257,0.067277284513851,-8.98924642641573E-17));
#5247=CARTESIAN_POINT('Origin',(0.,0.,0.));
#5248=CARTESIAN_POINT('',(-0.375277674973257,0.0768195421087395,-0.65));
#5249=CARTESIAN_POINT('Ctrl Pts',(-0.375277674973257,0.0768195421087395,
-0.65));
#5250=CARTESIAN_POINT('Ctrl Pts',(-0.562916512459968,-0.0315137912242437,
-0.324999999999856));
#5251=CARTESIAN_POINT('Ctrl Pts',(-0.750555349946514,0.0768195421087395,
-9.19165206894919E-17));
#5252=CARTESIAN_POINT('',(0.375277674973257,0.0768195421087395,-0.65));
#5253=CARTESIAN_POINT('Ctrl Pts',(0.375277674973257,0.0768195421087395,
-0.65));
#5254=CARTESIAN_POINT('Ctrl Pts',(-1.66144875635155E-13,-0.0315137912242437,
-0.65));
#5255=CARTESIAN_POINT('Ctrl Pts',(-0.375277674973257,0.0768195421087395,
-0.65));
#5256=CARTESIAN_POINT('',(0.750555349946514,0.0768195421087394,0.));
#5257=CARTESIAN_POINT('Ctrl Pts',(0.750555349946514,0.0768195421087394,
0.));
#5258=CARTESIAN_POINT('Ctrl Pts',(0.562916512459802,-0.0315137912242436,
-0.325000000000144));
#5259=CARTESIAN_POINT('Ctrl Pts',(0.375277674973257,0.0768195421087395,
-0.65));
#5260=CARTESIAN_POINT('Ctrl Pts',(0.375277674973257,0.0768195421087394,
0.65));
#5261=CARTESIAN_POINT('Ctrl Pts',(0.562916512459968,-0.0315137912242439,
0.324999999999856));
#5262=CARTESIAN_POINT('Ctrl Pts',(0.750555349946514,0.0768195421087394,
0.));
#5263=CARTESIAN_POINT('Origin',(0.,0.612722715486149,0.));
#5264=CARTESIAN_POINT('',(-0.6175,0.68,-7.5621939847349E-17));
#5265=CARTESIAN_POINT('Origin',(0.,0.68,0.));
#5266=CARTESIAN_POINT('',(-0.750555349946514,0.603180457891261,-9.19165206894919E-17));
#5267=CARTESIAN_POINT('',(-0.734027674973257,0.612722715486149,-8.98924642641573E-17));
#5268=CARTESIAN_POINT('',(-0.375277674973257,0.603180457891261,0.65));
#5269=CARTESIAN_POINT('Ctrl Pts',(-0.375277674973257,0.603180457891261,
0.65));
#5270=CARTESIAN_POINT('Ctrl Pts',(-0.562916512459968,0.711513791224243,
0.324999999999856));
#5271=CARTESIAN_POINT('Ctrl Pts',(-0.750555349946514,0.603180457891261,
-9.19165206894919E-17));
#5272=CARTESIAN_POINT('',(0.375277674973257,0.603180457891261,0.65));
#5273=CARTESIAN_POINT('Ctrl Pts',(0.375277674973257,0.603180457891261,0.65));
#5274=CARTESIAN_POINT('Ctrl Pts',(-1.66755498298699E-13,0.711513791224244,
0.65));
#5275=CARTESIAN_POINT('Ctrl Pts',(-0.375277674973257,0.603180457891261,
0.65));
#5276=CARTESIAN_POINT('',(0.750555349946514,0.603180457891261,0.));
#5277=CARTESIAN_POINT('Ctrl Pts',(0.750555349946514,0.603180457891261,0.));
#5278=CARTESIAN_POINT('Ctrl Pts',(0.562916512459802,0.711513791224244,0.325000000000144));
#5279=CARTESIAN_POINT('Ctrl Pts',(0.375277674973257,0.603180457891261,0.65));
#5280=CARTESIAN_POINT('',(0.375277674973257,0.603180457891261,-0.65));
#5281=CARTESIAN_POINT('Ctrl Pts',(0.375277674973257,0.603180457891261,-0.65));
#5282=CARTESIAN_POINT('Ctrl Pts',(0.562916512459969,0.711513791224244,-0.324999999999856));
#5283=CARTESIAN_POINT('Ctrl Pts',(0.750555349946514,0.603180457891261,0.));
#5284=CARTESIAN_POINT('',(-0.375277674973257,0.603180457891261,-0.65));
#5285=CARTESIAN_POINT('Ctrl Pts',(-0.375277674973257,0.603180457891261,
-0.65));
#5286=CARTESIAN_POINT('Ctrl Pts',(1.66422431391311E-13,0.711513791224244,
-0.65));
#5287=CARTESIAN_POINT('Ctrl Pts',(0.375277674973257,0.603180457891261,-0.65));
#5288=CARTESIAN_POINT('Ctrl Pts',(-0.750555349946514,0.603180457891261,
-9.19165206894919E-17));
#5289=CARTESIAN_POINT('Ctrl Pts',(-0.562916512459802,0.711513791224244,
-0.325000000000144));
#5290=CARTESIAN_POINT('Ctrl Pts',(-0.375277674973257,0.603180457891261,
-0.65));
#5291=CARTESIAN_POINT('Origin',(0.375277674973257,0.,-0.65));
#5292=CARTESIAN_POINT('',(-0.375277674973257,0.,-0.65));
#5293=CARTESIAN_POINT('',(0.375277674973257,0.,-0.65));
#5294=CARTESIAN_POINT('Origin',(-0.375277674973257,0.,-0.65));
#5295=CARTESIAN_POINT('',(-0.750555349946514,0.,-9.19165206894919E-17));
#5296=CARTESIAN_POINT('Origin',(-0.750555349946514,0.,-9.19165206894919E-17));
#5297=CARTESIAN_POINT('',(-0.375277674973257,0.,0.65));
#5298=CARTESIAN_POINT('Origin',(0.,0.,0.));
#5299=CARTESIAN_POINT('',(-0.338975,0.68,4.15124648740974E-17));
#5300=CARTESIAN_POINT('Origin',(0.,0.68,0.));
#5301=CARTESIAN_POINT('',(-0.338975,0.,4.15124648740974E-17));
#5302=CARTESIAN_POINT('Origin',(-0.375277674973257,0.,0.65));
#5303=CARTESIAN_POINT('',(0.375277674973257,0.,0.65));
#5304=CARTESIAN_POINT('Origin',(0.750555349946514,0.,0.));
#5305=CARTESIAN_POINT('',(0.750555349946514,0.,0.));
#5306=CARTESIAN_POINT('Origin',(0.375277674973257,0.,0.65));
#5307=CARTESIAN_POINT('Origin',(0.,0.68,-1.11022302462516E-16));
#5308=CARTESIAN_POINT('Origin',(0.,0.,-1.11022302462516E-16));
#5486=UNCERTAINTY_MEASURE_WITH_UNIT(LENGTH_MEASURE(0.001),#5503,
'DISTANCE_ACCURACY_VALUE',
'Maximum model space distance between geometric entities at asserted c
onnectivities');
#5489=UNCERTAINTY_MEASURE_WITH_UNIT(LENGTH_MEASURE(0.001),#5503,
'DISTANCE_ACCURACY_VALUE',
'Maximum model space distance between geometric entities at asserted c
onnectivities');
#5499=(
GEOMETRIC_REPRESENTATION_CONTEXT(3)
GLOBAL_UNCERTAINTY_ASSIGNED_CONTEXT((#5486))
GLOBAL_UNIT_ASSIGNED_CONTEXT((#5503,#5505,#5506))
REPRESENTATION_CONTEXT('','3D')
);
#5502=(
GEOMETRIC_REPRESENTATION_CONTEXT(3)
GLOBAL_UNCERTAINTY_ASSIGNED_CONTEXT((#5489))
GLOBAL_UNIT_ASSIGNED_CONTEXT((#5503,#5505,#5506))
REPRESENTATION_CONTEXT('','3D')
);
#5503=(
LENGTH_UNIT()
NAMED_UNIT(*)
SI_UNIT(.CENTI.,.METRE.)
);
#5505=(
NAMED_UNIT(*)
PLANE_ANGLE_UNIT()
SI_UNIT($,.RADIAN.)
);
#5506=(
NAMED_UNIT(*)
SI_UNIT($,.STERADIAN.)
SOLID_ANGLE_UNIT()
);
#5516=SHAPE_DEFINITION_REPRESENTATION(#5531,#5563);
#5531=PRODUCT_DEFINITION_SHAPE('',$,#5576);
#5563=SHAPE_REPRESENTATION('',(#3524),#5499);
#5566=PRODUCT_DEFINITION_CONTEXT('part definition',#5604,'design');
#5576=PRODUCT_DEFINITION('Hex Nut - M8','Hex Nut - M8',#5588,
#5566);
#5588=PRODUCT_DEFINITION_FORMATION('',$,#5615);
#5604=APPLICATION_CONTEXT(
'Core Data for Automotive Mechanical Design Process');
#5605=PRODUCT_CONTEXT('part definition',#5604,'mechanical');
#5615=PRODUCT('Hex Nut - M8','Hex Nut - M8','Hex Nut - M8',
(#5605));
#5695=COLOUR_RGB('Black',0.12,0.14,0.17);
#5696=FILL_AREA_STYLE_COLOUR('',#5695);
#5697=FILL_AREA_STYLE('',(#5696));
#5698=SURFACE_STYLE_FILL_AREA(#5697);
#5699=SURFACE_SIDE_STYLE('',(#5698));
#5700=SURFACE_STYLE_USAGE(.BOTH.,#5699);
#5701=PRESENTATION_STYLE_ASSIGNMENT((#5700));
ENDSEC;
END-ISO-10303-21;
